ISO-10303-21;
HEADER;
/* Generated by software containing ST-Developer
 * from STEP Tools, Inc. (www.steptools.com) 
 */

FILE_DESCRIPTION(
/* description */ (''),
/* implementation_level */ '2;1');

FILE_NAME(
/* name */ '20_Exhaust_Silencer_3-8.step',
/* time_stamp */ '2026-10-26T06:13:19-07:00',
/* author */ (''),
/* organization */ (''),
/* preprocessor_version */ 'ST-DEVELOPER v20.2',
/* originating_system */ 'Autodesk Translation Framework v15.15.0.0',
/* authorisation */ '');

FILE_SCHEMA (('AUTOMOTIVE_DESIGN { 1 0 10303 214 3 1 1 }','TECHNICAL_DATA_PACKAGING'));
ENDSEC;

DATA;
#10=MECHANICAL_DESIGN_GEOMETRIC_PRESENTATION_REPRESENTATION('',(#309),#56639);
#269=SHAPE_REPRESENTATION_RELATIONSHIP('SRR','None',#56757,#289);
#289=ADVANCED_BREP_SHAPE_REPRESENTATION('',(#329),#56631);
#309=STYLED_ITEM('',(#56901),#329);
#329=MANIFOLD_SOLID_BREP('Body1',#16961);
#539=FACE_BOUND('',#3422,.T.);
#540=FACE_BOUND('',#3431,.T.);
#541=FACE_BOUND('',#3433,.T.);
#542=FACE_BOUND('',#3435,.T.);
#543=FACE_BOUND('',#3439,.T.);
#544=FACE_BOUND('',#3441,.T.);
#616=CONICAL_SURFACE('',#18161,11.8232233047034,0.392699081698714);
#617=CONICAL_SURFACE('',#18166,11.25,0.785398163397447);
#618=CONICAL_SURFACE('',#18171,10.4267766952966,1.17809724509618);
#619=CONICAL_SURFACE('',#18174,11.75,0.785398163397451);
#620=CONICAL_SURFACE('',#18199,8.35,0.540419500270581);
#1104=CIRCLE('',#18160,8.5);
#1105=CIRCLE('',#18162,12.);
#1106=CIRCLE('',#18163,12.);
#1107=CIRCLE('',#18164,11.6464466094067);
#1108=CIRCLE('',#18165,11.6464466094067);
#1109=CIRCLE('',#18167,10.8535533905933);
#1110=CIRCLE('',#18168,10.8535533905933);
#1111=CIRCLE('',#18170,12.);
#1112=CIRCLE('',#18172,10.);
#1113=CIRCLE('',#18175,11.5);
#1114=CIRCLE('',#18176,12.);
#1115=CIRCLE('',#18177,12.);
#1116=CIRCLE('',#18179,12.);
#1117=CIRCLE('',#18182,11.);
#1118=CIRCLE('',#18184,12.);
#1119=CIRCLE('',#18185,11.);
#1120=CIRCLE('',#18188,12.);
#1121=CIRCLE('',#18190,11.);
#1122=CIRCLE('',#18192,11.);
#1123=CIRCLE('',#18198,8.5);
#1124=CIRCLE('',#18200,8.2);
#1448=CYLINDRICAL_SURFACE('',#18169,12.);
#1449=CYLINDRICAL_SURFACE('',#18178,12.);
#1450=CYLINDRICAL_SURFACE('',#18186,11.);
#1451=CYLINDRICAL_SURFACE('',#18187,12.);
#1452=CYLINDRICAL_SURFACE('',#18193,11.);
#1453=CYLINDRICAL_SURFACE('',#18197,8.5);
#2302=FACE_OUTER_BOUND('',#3400,.T.);
#2303=FACE_OUTER_BOUND('',#3401,.T.);
#2304=FACE_OUTER_BOUND('',#3402,.T.);
#2305=FACE_OUTER_BOUND('',#3403,.T.);
#2306=FACE_OUTER_BOUND('',#3404,.T.);
#2307=FACE_OUTER_BOUND('',#3405,.T.);
#2308=FACE_OUTER_BOUND('',#3406,.T.);
#2309=FACE_OUTER_BOUND('',#3407,.T.);
#2310=FACE_OUTER_BOUND('',#3408,.T.);
#2311=FACE_OUTER_BOUND('',#3409,.T.);
#2312=FACE_OUTER_BOUND('',#3410,.T.);
#2313=FACE_OUTER_BOUND('',#3411,.T.);
#2314=FACE_OUTER_BOUND('',#3412,.T.);
#2315=FACE_OUTER_BOUND('',#3413,.T.);
#2316=FACE_OUTER_BOUND('',#3414,.T.);
#2317=FACE_OUTER_BOUND('',#3415,.T.);
#2318=FACE_OUTER_BOUND('',#3416,.T.);
#2319=FACE_OUTER_BOUND('',#3417,.T.);
#2320=FACE_OUTER_BOUND('',#3418,.T.);
#2321=FACE_OUTER_BOUND('',#3419,.T.);
#2322=FACE_OUTER_BOUND('',#3420,.T.);
#2323=FACE_OUTER_BOUND('',#3421,.T.);
#2324=FACE_OUTER_BOUND('',#3423,.T.);
#2325=FACE_OUTER_BOUND('',#3424,.T.);
#2326=FACE_OUTER_BOUND('',#3425,.T.);
#2327=FACE_OUTER_BOUND('',#3426,.T.);
#2328=FACE_OUTER_BOUND('',#3427,.T.);
#2329=FACE_OUTER_BOUND('',#3428,.T.);
#2330=FACE_OUTER_BOUND('',#3429,.T.);
#2331=FACE_OUTER_BOUND('',#3430,.T.);
#2332=FACE_OUTER_BOUND('',#3432,.T.);
#2333=FACE_OUTER_BOUND('',#3434,.T.);
#2334=FACE_OUTER_BOUND('',#3436,.T.);
#2335=FACE_OUTER_BOUND('',#3437,.T.);
#2336=FACE_OUTER_BOUND('',#3438,.T.);
#2337=FACE_OUTER_BOUND('',#3440,.T.);
#2338=FACE_OUTER_BOUND('',#3442,.T.);
#2339=FACE_OUTER_BOUND('',#3443,.T.);
#2340=FACE_OUTER_BOUND('',#3444,.T.);
#2341=FACE_OUTER_BOUND('',#3445,.T.);
#2342=FACE_OUTER_BOUND('',#3446,.T.);
#2343=FACE_OUTER_BOUND('',#3447,.T.);
#2344=FACE_OUTER_BOUND('',#3448,.T.);
#3400=EDGE_LOOP('',(#13170,#13171,#13172));
#3401=EDGE_LOOP('',(#13173,#13174,#13175));
#3402=EDGE_LOOP('',(#13176,#13177,#13178));
#3403=EDGE_LOOP('',(#13179,#13180,#13181,#13182));
#3404=EDGE_LOOP('',(#13183,#13184,#13185));
#3405=EDGE_LOOP('',(#13186,#13187,#13188));
#3406=EDGE_LOOP('',(#13189,#13190,#13191));
#3407=EDGE_LOOP('',(#13192,#13193,#13194,#13195));
#3408=EDGE_LOOP('',(#13196,#13197,#13198,#13199));
#3409=EDGE_LOOP('',(#13200,#13201,#13202,#13203));
#3410=EDGE_LOOP('',(#13204,#13205,#13206,#13207));
#3411=EDGE_LOOP('',(#13208,#13209,#13210,#13211));
#3412=EDGE_LOOP('',(#13212,#13213,#13214,#13215));
#3413=EDGE_LOOP('',(#13216,#13217,#13218,#13219));
#3414=EDGE_LOOP('',(#13220,#13221,#13222,#13223));
#3415=EDGE_LOOP('',(#13224,#13225,#13226,#13227));
#3416=EDGE_LOOP('',(#13228,#13229,#13230,#13231));
#3417=EDGE_LOOP('',(#13232,#13233,#13234,#13235));
#3418=EDGE_LOOP('',(#13236,#13237,#13238,#13239));
#3419=EDGE_LOOP('',(#13240,#13241,#13242,#13243));
#3420=EDGE_LOOP('',(#13244,#13245,#13246,#13247));
#3421=EDGE_LOOP('',(#13248,#13249,#13250,#13251,#13252,#13253));
#3422=EDGE_LOOP('',(#13254));
#3423=EDGE_LOOP('',(#13255,#13256,#13257,#13258,#13259,#13260));
#3424=EDGE_LOOP('',(#13261,#13262,#13263,#13264,#13265,#13266));
#3425=EDGE_LOOP('',(#13267,#13268,#13269,#13270,#13271));
#3426=EDGE_LOOP('',(#13272,#13273,#13274,#13275,#13276));
#3427=EDGE_LOOP('',(#13277));
#3428=EDGE_LOOP('',(#13278,#13279,#13280,#13281,#13282));
#3429=EDGE_LOOP('',(#13283,#13284,#13285,#13286,#13287));
#3430=EDGE_LOOP('',(#13288));
#3431=EDGE_LOOP('',(#13289,#13290,#13291,#13292,#13293,#13294,#13295,#13296,
#13297,#13298,#13299,#13300));
#3432=EDGE_LOOP('',(#13301));
#3433=EDGE_LOOP('',(#13302));
#3434=EDGE_LOOP('',(#13303));
#3435=EDGE_LOOP('',(#13304));
#3436=EDGE_LOOP('',(#13305,#13306,#13307,#13308));
#3437=EDGE_LOOP('',(#13309,#13310,#13311,#13312));
#3438=EDGE_LOOP('',(#13313));
#3439=EDGE_LOOP('',(#13314));
#3440=EDGE_LOOP('',(#13315));
#3441=EDGE_LOOP('',(#13316));
#3442=EDGE_LOOP('',(#13317,#13318,#13319,#13320));
#3443=EDGE_LOOP('',(#13321,#13322,#13323,#13324));
#3444=EDGE_LOOP('',(#13325,#13326,#13327,#13328));
#3445=EDGE_LOOP('',(#13329,#13330,#13331,#13332));
#3446=EDGE_LOOP('',(#13333,#13334,#13335,#13336));
#3447=EDGE_LOOP('',(#13337,#13338,#13339,#13340));
#3448=EDGE_LOOP('',(#13341));
#4356=LINE('',#36251,#5310);
#4357=LINE('',#36253,#5311);
#4358=LINE('',#36254,#5312);
#4359=LINE('',#36258,#5313);
#4360=LINE('',#36260,#5314);
#4361=LINE('',#36261,#5315);
#4362=LINE('',#36265,#5316);
#4363=LINE('',#36267,#5317);
#4364=LINE('',#36268,#5318);
#4365=LINE('',#36270,#5319);
#4366=LINE('',#36271,#5320);
#4367=LINE('',#36275,#5321);
#4368=LINE('',#36277,#5322);
#4369=LINE('',#36278,#5323);
#4370=LINE('',#36282,#5324);
#4371=LINE('',#36284,#5325);
#4372=LINE('',#36285,#5326);
#4373=LINE('',#36289,#5327);
#4374=LINE('',#36291,#5328);
#4375=LINE('',#36292,#5329);
#4376=LINE('',#36294,#5330);
#4377=LINE('',#36295,#5331);
#4378=LINE('',#36297,#5332);
#4379=LINE('',#36298,#5333);
#4380=LINE('',#36302,#5334);
#4381=LINE('',#36303,#5335);
#4382=LINE('',#36304,#5336);
#4383=LINE('',#36308,#5337);
#4384=LINE('',#36309,#5338);
#4385=LINE('',#36310,#5339);
#4386=LINE('',#36312,#5340);
#4387=LINE('',#36313,#5341);
#4388=LINE('',#36315,#5342);
#4389=LINE('',#36316,#5343);
#4390=LINE('',#36320,#5344);
#4391=LINE('',#36321,#5345);
#4392=LINE('',#36322,#5346);
#4393=LINE('',#36326,#5347);
#4394=LINE('',#36327,#5348);
#4395=LINE('',#36328,#5349);
#4396=LINE('',#36330,#5350);
#4397=LINE('',#36331,#5351);
#4398=LINE('',#36335,#5352);
#4399=LINE('',#36336,#5353);
#4400=LINE('',#36337,#5354);
#4401=LINE('',#36341,#5355);
#4402=LINE('',#36342,#5356);
#4403=LINE('',#36343,#5357);
#4404=LINE('',#36345,#5358);
#4405=LINE('',#36347,#5359);
#4406=LINE('',#36349,#5360);
#4407=LINE('',#36359,#5361);
#4408=LINE('',#36365,#5362);
#4409=LINE('',#36372,#5363);
#4410=LINE('',#36375,#5364);
#4411=LINE('',#36382,#5365);
#4412=LINE('',#36388,#5366);
#4413=LINE('',#36391,#5367);
#4414=LINE('',#36392,#5368);
#4415=LINE('',#36393,#5369);
#4416=LINE('',#36403,#5370);
#4417=LINE('',#36407,#5371);
#4418=LINE('',#36415,#5372);
#4419=LINE('',#36422,#5373);
#4420=LINE('',#36426,#5374);
#5310=VECTOR('',#21142,10.);
#5311=VECTOR('',#21143,10.);
#5312=VECTOR('',#21144,10.);
#5313=VECTOR('',#21147,10.);
#5314=VECTOR('',#21148,10.);
#5315=VECTOR('',#21149,10.);
#5316=VECTOR('',#21152,10.);
#5317=VECTOR('',#21153,10.);
#5318=VECTOR('',#21154,10.);
#5319=VECTOR('',#21157,10.);
#5320=VECTOR('',#21158,10.);
#5321=VECTOR('',#21161,10.);
#5322=VECTOR('',#21162,10.);
#5323=VECTOR('',#21163,10.);
#5324=VECTOR('',#21166,10.);
#5325=VECTOR('',#21167,10.);
#5326=VECTOR('',#21168,10.);
#5327=VECTOR('',#21171,10.);
#5328=VECTOR('',#21172,10.);
#5329=VECTOR('',#21173,10.);
#5330=VECTOR('',#21176,10.);
#5331=VECTOR('',#21177,10.);
#5332=VECTOR('',#21180,10.);
#5333=VECTOR('',#21181,10.);
#5334=VECTOR('',#21184,10.);
#5335=VECTOR('',#21185,10.);
#5336=VECTOR('',#21186,10.);
#5337=VECTOR('',#21189,10.);
#5338=VECTOR('',#21190,10.);
#5339=VECTOR('',#21191,10.);
#5340=VECTOR('',#21194,10.);
#5341=VECTOR('',#21195,10.);
#5342=VECTOR('',#21198,10.);
#5343=VECTOR('',#21199,10.);
#5344=VECTOR('',#21202,10.);
#5345=VECTOR('',#21203,10.);
#5346=VECTOR('',#21204,10.);
#5347=VECTOR('',#21207,10.);
#5348=VECTOR('',#21208,10.);
#5349=VECTOR('',#21209,10.);
#5350=VECTOR('',#21212,10.);
#5351=VECTOR('',#21213,10.);
#5352=VECTOR('',#21216,10.);
#5353=VECTOR('',#21217,10.);
#5354=VECTOR('',#21218,10.);
#5355=VECTOR('',#21221,10.);
#5356=VECTOR('',#21222,10.);
#5357=VECTOR('',#21223,10.);
#5358=VECTOR('',#21226,10.);
#5359=VECTOR('',#21229,10.);
#5360=VECTOR('',#21232,10.);
#5361=VECTOR('',#21243,11.8232233047034);
#5362=VECTOR('',#21250,11.25);
#5363=VECTOR('',#21259,12.);
#5364=VECTOR('',#21262,10.4267766952966);
#5365=VECTOR('',#21271,11.75);
#5366=VECTOR('',#21278,12.);
#5367=VECTOR('',#21283,10.);
#5368=VECTOR('',#21284,10.);
#5369=VECTOR('',#21285,10.);
#5370=VECTOR('',#21298,11.);
#5371=VECTOR('',#21303,12.);
#5372=VECTOR('',#21314,11.);
#5373=VECTOR('',#21325,8.5);
#5374=VECTOR('',#21330,8.35);
#7468=VERTEX_POINT('',#36249);
#7469=VERTEX_POINT('',#36250);
#7470=VERTEX_POINT('',#36252);
#7471=VERTEX_POINT('',#36256);
#7472=VERTEX_POINT('',#36257);
#7473=VERTEX_POINT('',#36259);
#7474=VERTEX_POINT('',#36263);
#7475=VERTEX_POINT('',#36264);
#7476=VERTEX_POINT('',#36266);
#7477=VERTEX_POINT('',#36273);
#7478=VERTEX_POINT('',#36274);
#7479=VERTEX_POINT('',#36276);
#7480=VERTEX_POINT('',#36280);
#7481=VERTEX_POINT('',#36281);
#7482=VERTEX_POINT('',#36283);
#7483=VERTEX_POINT('',#36287);
#7484=VERTEX_POINT('',#36288);
#7485=VERTEX_POINT('',#36290);
#7486=VERTEX_POINT('',#36300);
#7487=VERTEX_POINT('',#36301);
#7488=VERTEX_POINT('',#36306);
#7489=VERTEX_POINT('',#36307);
#7490=VERTEX_POINT('',#36318);
#7491=VERTEX_POINT('',#36319);
#7492=VERTEX_POINT('',#36324);
#7493=VERTEX_POINT('',#36325);
#7494=VERTEX_POINT('',#36333);
#7495=VERTEX_POINT('',#36334);
#7496=VERTEX_POINT('',#36339);
#7497=VERTEX_POINT('',#36340);
#7498=VERTEX_POINT('',#36351);
#7499=VERTEX_POINT('',#36354);
#7500=VERTEX_POINT('',#36355);
#7501=VERTEX_POINT('',#36358);
#7502=VERTEX_POINT('',#36360);
#7503=VERTEX_POINT('',#36364);
#7504=VERTEX_POINT('',#36366);
#7505=VERTEX_POINT('',#36370);
#7506=VERTEX_POINT('',#36374);
#7507=VERTEX_POINT('',#36379);
#7508=VERTEX_POINT('',#36381);
#7509=VERTEX_POINT('',#36383);
#7510=VERTEX_POINT('',#36387);
#7511=VERTEX_POINT('',#36395);
#7512=VERTEX_POINT('',#36398);
#7513=VERTEX_POINT('',#36400);
#7514=VERTEX_POINT('',#36405);
#7515=VERTEX_POINT('',#36409);
#7516=VERTEX_POINT('',#36412);
#7517=VERTEX_POINT('',#36420);
#7518=VERTEX_POINT('',#36424);
#9492=EDGE_CURVE('',#7468,#7469,#4356,.T.);
#9493=EDGE_CURVE('',#7470,#7468,#4357,.T.);
#9494=EDGE_CURVE('',#7469,#7470,#4358,.T.);
#9495=EDGE_CURVE('',#7471,#7472,#4359,.T.);
#9496=EDGE_CURVE('',#7473,#7471,#4360,.T.);
#9497=EDGE_CURVE('',#7472,#7473,#4361,.T.);
#9498=EDGE_CURVE('',#7474,#7475,#4362,.T.);
#9499=EDGE_CURVE('',#7476,#7474,#4363,.T.);
#9500=EDGE_CURVE('',#7475,#7476,#4364,.T.);
#9501=EDGE_CURVE('',#7470,#7476,#4365,.T.);
#9502=EDGE_CURVE('',#7474,#7469,#4366,.T.);
#9503=EDGE_CURVE('',#7477,#7478,#4367,.T.);
#9504=EDGE_CURVE('',#7479,#7477,#4368,.T.);
#9505=EDGE_CURVE('',#7478,#7479,#4369,.T.);
#9506=EDGE_CURVE('',#7480,#7481,#4370,.T.);
#9507=EDGE_CURVE('',#7482,#7480,#4371,.T.);
#9508=EDGE_CURVE('',#7481,#7482,#4372,.T.);
#9509=EDGE_CURVE('',#7483,#7484,#4373,.T.);
#9510=EDGE_CURVE('',#7485,#7483,#4374,.T.);
#9511=EDGE_CURVE('',#7484,#7485,#4375,.T.);
#9512=EDGE_CURVE('',#7480,#7485,#4376,.T.);
#9513=EDGE_CURVE('',#7483,#7482,#4377,.T.);
#9514=EDGE_CURVE('',#7485,#7479,#4378,.T.);
#9515=EDGE_CURVE('',#7477,#7484,#4379,.T.);
#9516=EDGE_CURVE('',#7486,#7487,#4380,.F.);
#9517=EDGE_CURVE('',#7487,#7483,#4381,.T.);
#9518=EDGE_CURVE('',#7484,#7486,#4382,.T.);
#9519=EDGE_CURVE('',#7488,#7489,#4383,.F.);
#9520=EDGE_CURVE('',#7489,#7481,#4384,.T.);
#9521=EDGE_CURVE('',#7482,#7488,#4385,.T.);
#9522=EDGE_CURVE('',#7476,#7480,#4386,.T.);
#9523=EDGE_CURVE('',#7481,#7475,#4387,.T.);
#9524=EDGE_CURVE('',#7479,#7473,#4388,.T.);
#9525=EDGE_CURVE('',#7471,#7478,#4389,.T.);
#9526=EDGE_CURVE('',#7490,#7491,#4390,.F.);
#9527=EDGE_CURVE('',#7491,#7477,#4391,.T.);
#9528=EDGE_CURVE('',#7478,#7490,#4392,.T.);
#9529=EDGE_CURVE('',#7492,#7493,#4393,.F.);
#9530=EDGE_CURVE('',#7493,#7474,#4394,.T.);
#9531=EDGE_CURVE('',#7475,#7492,#4395,.T.);
#9532=EDGE_CURVE('',#7473,#7470,#4396,.T.);
#9533=EDGE_CURVE('',#7468,#7472,#4397,.T.);
#9534=EDGE_CURVE('',#7494,#7495,#4398,.F.);
#9535=EDGE_CURVE('',#7495,#7471,#4399,.T.);
#9536=EDGE_CURVE('',#7472,#7494,#4400,.T.);
#9537=EDGE_CURVE('',#7496,#7497,#4401,.F.);
#9538=EDGE_CURVE('',#7497,#7468,#4402,.T.);
#9539=EDGE_CURVE('',#7469,#7496,#4403,.T.);
#9540=EDGE_CURVE('',#7486,#7491,#4404,.T.);
#9541=EDGE_CURVE('',#7490,#7495,#4405,.T.);
#9542=EDGE_CURVE('',#7494,#7497,#4406,.T.);
#9543=EDGE_CURVE('',#7498,#7498,#1104,.T.);
#9544=EDGE_CURVE('',#7499,#7500,#1105,.T.);
#9545=EDGE_CURVE('',#7500,#7499,#1106,.T.);
#9546=EDGE_CURVE('',#7499,#7501,#4407,.T.);
#9547=EDGE_CURVE('',#7501,#7502,#1107,.T.);
#9548=EDGE_CURVE('',#7502,#7501,#1108,.T.);
#9549=EDGE_CURVE('',#7502,#7503,#4408,.T.);
#9550=EDGE_CURVE('',#7504,#7503,#1109,.T.);
#9551=EDGE_CURVE('',#7503,#7504,#1110,.T.);
#9552=EDGE_CURVE('',#7505,#7505,#1111,.T.);
#9553=EDGE_CURVE('',#7505,#7500,#4409,.T.);
#9554=EDGE_CURVE('',#7504,#7506,#4410,.T.);
#9555=EDGE_CURVE('',#7506,#7506,#1112,.T.);
#9556=EDGE_CURVE('',#7507,#7507,#1113,.T.);
#9557=EDGE_CURVE('',#7507,#7508,#4411,.T.);
#9558=EDGE_CURVE('',#7508,#7509,#1114,.T.);
#9559=EDGE_CURVE('',#7509,#7508,#1115,.T.);
#9560=EDGE_CURVE('',#7509,#7510,#4412,.T.);
#9561=EDGE_CURVE('',#7510,#7510,#1116,.T.);
#9562=EDGE_CURVE('',#7492,#7489,#4413,.T.);
#9563=EDGE_CURVE('',#7488,#7487,#4414,.T.);
#9564=EDGE_CURVE('',#7496,#7493,#4415,.T.);
#9565=EDGE_CURVE('',#7511,#7511,#1117,.T.);
#9566=EDGE_CURVE('',#7512,#7512,#1118,.T.);
#9567=EDGE_CURVE('',#7513,#7513,#1119,.T.);
#9568=EDGE_CURVE('',#7511,#7513,#4416,.T.);
#9569=EDGE_CURVE('',#7514,#7514,#1120,.T.);
#9570=EDGE_CURVE('',#7514,#7512,#4417,.T.);
#9571=EDGE_CURVE('',#7515,#7515,#1121,.T.);
#9572=EDGE_CURVE('',#7516,#7516,#1122,.T.);
#9573=EDGE_CURVE('',#7515,#7516,#4418,.T.);
#9574=EDGE_CURVE('',#7517,#7517,#1123,.T.);
#9575=EDGE_CURVE('',#7517,#7498,#4419,.T.);
#9576=EDGE_CURVE('',#7518,#7518,#1124,.T.);
#9577=EDGE_CURVE('',#7518,#7517,#4420,.T.);
#13170=ORIENTED_EDGE('',*,*,#9492,.F.);
#13171=ORIENTED_EDGE('',*,*,#9493,.F.);
#13172=ORIENTED_EDGE('',*,*,#9494,.F.);
#13173=ORIENTED_EDGE('',*,*,#9495,.F.);
#13174=ORIENTED_EDGE('',*,*,#9496,.F.);
#13175=ORIENTED_EDGE('',*,*,#9497,.F.);
#13176=ORIENTED_EDGE('',*,*,#9498,.F.);
#13177=ORIENTED_EDGE('',*,*,#9499,.F.);
#13178=ORIENTED_EDGE('',*,*,#9500,.F.);
#13179=ORIENTED_EDGE('',*,*,#9494,.T.);
#13180=ORIENTED_EDGE('',*,*,#9501,.T.);
#13181=ORIENTED_EDGE('',*,*,#9499,.T.);
#13182=ORIENTED_EDGE('',*,*,#9502,.T.);
#13183=ORIENTED_EDGE('',*,*,#9503,.F.);
#13184=ORIENTED_EDGE('',*,*,#9504,.F.);
#13185=ORIENTED_EDGE('',*,*,#9505,.F.);
#13186=ORIENTED_EDGE('',*,*,#9506,.F.);
#13187=ORIENTED_EDGE('',*,*,#9507,.F.);
#13188=ORIENTED_EDGE('',*,*,#9508,.F.);
#13189=ORIENTED_EDGE('',*,*,#9509,.F.);
#13190=ORIENTED_EDGE('',*,*,#9510,.F.);
#13191=ORIENTED_EDGE('',*,*,#9511,.F.);
#13192=ORIENTED_EDGE('',*,*,#9507,.T.);
#13193=ORIENTED_EDGE('',*,*,#9512,.T.);
#13194=ORIENTED_EDGE('',*,*,#9510,.T.);
#13195=ORIENTED_EDGE('',*,*,#9513,.T.);
#13196=ORIENTED_EDGE('',*,*,#9511,.T.);
#13197=ORIENTED_EDGE('',*,*,#9514,.T.);
#13198=ORIENTED_EDGE('',*,*,#9504,.T.);
#13199=ORIENTED_EDGE('',*,*,#9515,.T.);
#13200=ORIENTED_EDGE('',*,*,#9516,.T.);
#13201=ORIENTED_EDGE('',*,*,#9517,.T.);
#13202=ORIENTED_EDGE('',*,*,#9509,.T.);
#13203=ORIENTED_EDGE('',*,*,#9518,.T.);
#13204=ORIENTED_EDGE('',*,*,#9519,.T.);
#13205=ORIENTED_EDGE('',*,*,#9520,.T.);
#13206=ORIENTED_EDGE('',*,*,#9508,.T.);
#13207=ORIENTED_EDGE('',*,*,#9521,.T.);
#13208=ORIENTED_EDGE('',*,*,#9500,.T.);
#13209=ORIENTED_EDGE('',*,*,#9522,.T.);
#13210=ORIENTED_EDGE('',*,*,#9506,.T.);
#13211=ORIENTED_EDGE('',*,*,#9523,.T.);
#13212=ORIENTED_EDGE('',*,*,#9505,.T.);
#13213=ORIENTED_EDGE('',*,*,#9524,.T.);
#13214=ORIENTED_EDGE('',*,*,#9496,.T.);
#13215=ORIENTED_EDGE('',*,*,#9525,.T.);
#13216=ORIENTED_EDGE('',*,*,#9526,.T.);
#13217=ORIENTED_EDGE('',*,*,#9527,.T.);
#13218=ORIENTED_EDGE('',*,*,#9503,.T.);
#13219=ORIENTED_EDGE('',*,*,#9528,.T.);
#13220=ORIENTED_EDGE('',*,*,#9529,.T.);
#13221=ORIENTED_EDGE('',*,*,#9530,.T.);
#13222=ORIENTED_EDGE('',*,*,#9498,.T.);
#13223=ORIENTED_EDGE('',*,*,#9531,.T.);
#13224=ORIENTED_EDGE('',*,*,#9497,.T.);
#13225=ORIENTED_EDGE('',*,*,#9532,.T.);
#13226=ORIENTED_EDGE('',*,*,#9493,.T.);
#13227=ORIENTED_EDGE('',*,*,#9533,.T.);
#13228=ORIENTED_EDGE('',*,*,#9534,.T.);
#13229=ORIENTED_EDGE('',*,*,#9535,.T.);
#13230=ORIENTED_EDGE('',*,*,#9495,.T.);
#13231=ORIENTED_EDGE('',*,*,#9536,.T.);
#13232=ORIENTED_EDGE('',*,*,#9537,.T.);
#13233=ORIENTED_EDGE('',*,*,#9538,.T.);
#13234=ORIENTED_EDGE('',*,*,#9492,.T.);
#13235=ORIENTED_EDGE('',*,*,#9539,.T.);
#13236=ORIENTED_EDGE('',*,*,#9518,.F.);
#13237=ORIENTED_EDGE('',*,*,#9515,.F.);
#13238=ORIENTED_EDGE('',*,*,#9527,.F.);
#13239=ORIENTED_EDGE('',*,*,#9540,.F.);
#13240=ORIENTED_EDGE('',*,*,#9528,.F.);
#13241=ORIENTED_EDGE('',*,*,#9525,.F.);
#13242=ORIENTED_EDGE('',*,*,#9535,.F.);
#13243=ORIENTED_EDGE('',*,*,#9541,.F.);
#13244=ORIENTED_EDGE('',*,*,#9536,.F.);
#13245=ORIENTED_EDGE('',*,*,#9533,.F.);
#13246=ORIENTED_EDGE('',*,*,#9538,.F.);
#13247=ORIENTED_EDGE('',*,*,#9542,.F.);
#13248=ORIENTED_EDGE('',*,*,#9512,.F.);
#13249=ORIENTED_EDGE('',*,*,#9522,.F.);
#13250=ORIENTED_EDGE('',*,*,#9501,.F.);
#13251=ORIENTED_EDGE('',*,*,#9532,.F.);
#13252=ORIENTED_EDGE('',*,*,#9524,.F.);
#13253=ORIENTED_EDGE('',*,*,#9514,.F.);
#13254=ORIENTED_EDGE('',*,*,#9543,.F.);
#13255=ORIENTED_EDGE('',*,*,#9544,.T.);
#13256=ORIENTED_EDGE('',*,*,#9545,.T.);
#13257=ORIENTED_EDGE('',*,*,#9546,.T.);
#13258=ORIENTED_EDGE('',*,*,#9547,.T.);
#13259=ORIENTED_EDGE('',*,*,#9548,.T.);
#13260=ORIENTED_EDGE('',*,*,#9546,.F.);
#13261=ORIENTED_EDGE('',*,*,#9547,.F.);
#13262=ORIENTED_EDGE('',*,*,#9548,.F.);
#13263=ORIENTED_EDGE('',*,*,#9549,.T.);
#13264=ORIENTED_EDGE('',*,*,#9550,.F.);
#13265=ORIENTED_EDGE('',*,*,#9551,.F.);
#13266=ORIENTED_EDGE('',*,*,#9549,.F.);
#13267=ORIENTED_EDGE('',*,*,#9552,.T.);
#13268=ORIENTED_EDGE('',*,*,#9553,.T.);
#13269=ORIENTED_EDGE('',*,*,#9544,.F.);
#13270=ORIENTED_EDGE('',*,*,#9545,.F.);
#13271=ORIENTED_EDGE('',*,*,#9553,.F.);
#13272=ORIENTED_EDGE('',*,*,#9550,.T.);
#13273=ORIENTED_EDGE('',*,*,#9551,.T.);
#13274=ORIENTED_EDGE('',*,*,#9554,.T.);
#13275=ORIENTED_EDGE('',*,*,#9555,.T.);
#13276=ORIENTED_EDGE('',*,*,#9554,.F.);
#13277=ORIENTED_EDGE('',*,*,#9555,.F.);
#13278=ORIENTED_EDGE('',*,*,#9556,.T.);
#13279=ORIENTED_EDGE('',*,*,#9557,.T.);
#13280=ORIENTED_EDGE('',*,*,#9558,.T.);
#13281=ORIENTED_EDGE('',*,*,#9559,.T.);
#13282=ORIENTED_EDGE('',*,*,#9557,.F.);
#13283=ORIENTED_EDGE('',*,*,#9558,.F.);
#13284=ORIENTED_EDGE('',*,*,#9559,.F.);
#13285=ORIENTED_EDGE('',*,*,#9560,.T.);
#13286=ORIENTED_EDGE('',*,*,#9561,.T.);
#13287=ORIENTED_EDGE('',*,*,#9560,.F.);
#13288=ORIENTED_EDGE('',*,*,#9556,.F.);
#13289=ORIENTED_EDGE('',*,*,#9562,.T.);
#13290=ORIENTED_EDGE('',*,*,#9519,.F.);
#13291=ORIENTED_EDGE('',*,*,#9563,.T.);
#13292=ORIENTED_EDGE('',*,*,#9516,.F.);
#13293=ORIENTED_EDGE('',*,*,#9540,.T.);
#13294=ORIENTED_EDGE('',*,*,#9526,.F.);
#13295=ORIENTED_EDGE('',*,*,#9541,.T.);
#13296=ORIENTED_EDGE('',*,*,#9534,.F.);
#13297=ORIENTED_EDGE('',*,*,#9542,.T.);
#13298=ORIENTED_EDGE('',*,*,#9537,.F.);
#13299=ORIENTED_EDGE('',*,*,#9564,.T.);
#13300=ORIENTED_EDGE('',*,*,#9529,.F.);
#13301=ORIENTED_EDGE('',*,*,#9552,.F.);
#13302=ORIENTED_EDGE('',*,*,#9565,.F.);
#13303=ORIENTED_EDGE('',*,*,#9566,.F.);
#13304=ORIENTED_EDGE('',*,*,#9567,.T.);
#13305=ORIENTED_EDGE('',*,*,#9565,.T.);
#13306=ORIENTED_EDGE('',*,*,#9568,.T.);
#13307=ORIENTED_EDGE('',*,*,#9567,.F.);
#13308=ORIENTED_EDGE('',*,*,#9568,.F.);
#13309=ORIENTED_EDGE('',*,*,#9569,.T.);
#13310=ORIENTED_EDGE('',*,*,#9570,.T.);
#13311=ORIENTED_EDGE('',*,*,#9566,.T.);
#13312=ORIENTED_EDGE('',*,*,#9570,.F.);
#13313=ORIENTED_EDGE('',*,*,#9569,.F.);
#13314=ORIENTED_EDGE('',*,*,#9571,.F.);
#13315=ORIENTED_EDGE('',*,*,#9561,.F.);
#13316=ORIENTED_EDGE('',*,*,#9572,.T.);
#13317=ORIENTED_EDGE('',*,*,#9571,.T.);
#13318=ORIENTED_EDGE('',*,*,#9573,.T.);
#13319=ORIENTED_EDGE('',*,*,#9572,.F.);
#13320=ORIENTED_EDGE('',*,*,#9573,.F.);
#13321=ORIENTED_EDGE('',*,*,#9520,.F.);
#13322=ORIENTED_EDGE('',*,*,#9562,.F.);
#13323=ORIENTED_EDGE('',*,*,#9531,.F.);
#13324=ORIENTED_EDGE('',*,*,#9523,.F.);
#13325=ORIENTED_EDGE('',*,*,#9530,.F.);
#13326=ORIENTED_EDGE('',*,*,#9564,.F.);
#13327=ORIENTED_EDGE('',*,*,#9539,.F.);
#13328=ORIENTED_EDGE('',*,*,#9502,.F.);
#13329=ORIENTED_EDGE('',*,*,#9517,.F.);
#13330=ORIENTED_EDGE('',*,*,#9563,.F.);
#13331=ORIENTED_EDGE('',*,*,#9521,.F.);
#13332=ORIENTED_EDGE('',*,*,#9513,.F.);
#13333=ORIENTED_EDGE('',*,*,#9574,.F.);
#13334=ORIENTED_EDGE('',*,*,#9575,.T.);
#13335=ORIENTED_EDGE('',*,*,#9543,.T.);
#13336=ORIENTED_EDGE('',*,*,#9575,.F.);
#13337=ORIENTED_EDGE('',*,*,#9576,.F.);
#13338=ORIENTED_EDGE('',*,*,#9577,.T.);
#13339=ORIENTED_EDGE('',*,*,#9574,.T.);
#13340=ORIENTED_EDGE('',*,*,#9577,.F.);
#13341=ORIENTED_EDGE('',*,*,#9576,.T.);
#15872=PLANE('',#18138);
#15873=PLANE('',#18139);
#15874=PLANE('',#18140);
#15875=PLANE('',#18141);
#15876=PLANE('',#18142);
#15877=PLANE('',#18143);
#15878=PLANE('',#18144);
#15879=PLANE('',#18145);
#15880=PLANE('',#18146);
#15881=PLANE('',#18147);
#15882=PLANE('',#18148);
#15883=PLANE('',#18149);
#15884=PLANE('',#18150);
#15885=PLANE('',#18151);
#15886=PLANE('',#18152);
#15887=PLANE('',#18153);
#15888=PLANE('',#18154);
#15889=PLANE('',#18155);
#15890=PLANE('',#18156);
#15891=PLANE('',#18157);
#15892=PLANE('',#18158);
#15893=PLANE('',#18159);
#15894=PLANE('',#18173);
#15895=PLANE('',#18180);
#15896=PLANE('',#18181);
#15897=PLANE('',#18183);
#15898=PLANE('',#18189);
#15899=PLANE('',#18191);
#15900=PLANE('',#18194);
#15901=PLANE('',#18195);
#15902=PLANE('',#18196);
#15903=PLANE('',#18201);
#16473=ADVANCED_FACE('',(#2302),#15872,.T.);
#16474=ADVANCED_FACE('',(#2303),#15873,.T.);
#16475=ADVANCED_FACE('',(#2304),#15874,.T.);
#16476=ADVANCED_FACE('',(#2305),#15875,.T.);
#16477=ADVANCED_FACE('',(#2306),#15876,.T.);
#16478=ADVANCED_FACE('',(#2307),#15877,.T.);
#16479=ADVANCED_FACE('',(#2308),#15878,.T.);
#16480=ADVANCED_FACE('',(#2309),#15879,.T.);
#16481=ADVANCED_FACE('',(#2310),#15880,.T.);
#16482=ADVANCED_FACE('',(#2311),#15881,.T.);
#16483=ADVANCED_FACE('',(#2312),#15882,.T.);
#16484=ADVANCED_FACE('',(#2313),#15883,.T.);
#16485=ADVANCED_FACE('',(#2314),#15884,.T.);
#16486=ADVANCED_FACE('',(#2315),#15885,.T.);
#16487=ADVANCED_FACE('',(#2316),#15886,.T.);
#16488=ADVANCED_FACE('',(#2317),#15887,.T.);
#16489=ADVANCED_FACE('',(#2318),#15888,.T.);
#16490=ADVANCED_FACE('',(#2319),#15889,.T.);
#16491=ADVANCED_FACE('',(#2320),#15890,.T.);
#16492=ADVANCED_FACE('',(#2321),#15891,.T.);
#16493=ADVANCED_FACE('',(#2322),#15892,.T.);
#16494=ADVANCED_FACE('',(#2323,#539),#15893,.F.);
#16495=ADVANCED_FACE('',(#2324),#616,.T.);
#16496=ADVANCED_FACE('',(#2325),#617,.T.);
#16497=ADVANCED_FACE('',(#2326),#1448,.T.);
#16498=ADVANCED_FACE('',(#2327),#618,.T.);
#16499=ADVANCED_FACE('',(#2328),#15894,.T.);
#16500=ADVANCED_FACE('',(#2329),#619,.T.);
#16501=ADVANCED_FACE('',(#2330),#1449,.T.);
#16502=ADVANCED_FACE('',(#2331,#540),#15895,.T.);
#16503=ADVANCED_FACE('',(#2332,#541),#15896,.F.);
#16504=ADVANCED_FACE('',(#2333,#542),#15897,.F.);
#16505=ADVANCED_FACE('',(#2334),#1450,.T.);
#16506=ADVANCED_FACE('',(#2335),#1451,.T.);
#16507=ADVANCED_FACE('',(#2336,#543),#15898,.F.);
#16508=ADVANCED_FACE('',(#2337,#544),#15899,.F.);
#16509=ADVANCED_FACE('',(#2338),#1452,.T.);
#16510=ADVANCED_FACE('',(#2339),#15900,.T.);
#16511=ADVANCED_FACE('',(#2340),#15901,.T.);
#16512=ADVANCED_FACE('',(#2341),#15902,.T.);
#16513=ADVANCED_FACE('',(#2342),#1453,.T.);
#16514=ADVANCED_FACE('',(#2343),#620,.T.);
#16515=ADVANCED_FACE('',(#2344),#15903,.T.);
#16961=CLOSED_SHELL('',(#16473,#16474,#16475,#16476,#16477,#16478,#16479,
#16480,#16481,#16482,#16483,#16484,#16485,#16486,#16487,#16488,#16489,#16490,
#16491,#16492,#16493,#16494,#16495,#16496,#16497,#16498,#16499,#16500,#16501,
#16502,#16503,#16504,#16505,#16506,#16507,#16508,#16509,#16510,#16511,#16512,
#16513,#16514,#16515));
#18137=AXIS2_PLACEMENT_3D('',#36247,#21138,#21139);
#18138=AXIS2_PLACEMENT_3D('',#36248,#21140,#21141);
#18139=AXIS2_PLACEMENT_3D('',#36255,#21145,#21146);
#18140=AXIS2_PLACEMENT_3D('',#36262,#21150,#21151);
#18141=AXIS2_PLACEMENT_3D('',#36269,#21155,#21156);
#18142=AXIS2_PLACEMENT_3D('',#36272,#21159,#21160);
#18143=AXIS2_PLACEMENT_3D('',#36279,#21164,#21165);
#18144=AXIS2_PLACEMENT_3D('',#36286,#21169,#21170);
#18145=AXIS2_PLACEMENT_3D('',#36293,#21174,#21175);
#18146=AXIS2_PLACEMENT_3D('',#36296,#21178,#21179);
#18147=AXIS2_PLACEMENT_3D('',#36299,#21182,#21183);
#18148=AXIS2_PLACEMENT_3D('',#36305,#21187,#21188);
#18149=AXIS2_PLACEMENT_3D('',#36311,#21192,#21193);
#18150=AXIS2_PLACEMENT_3D('',#36314,#21196,#21197);
#18151=AXIS2_PLACEMENT_3D('',#36317,#21200,#21201);
#18152=AXIS2_PLACEMENT_3D('',#36323,#21205,#21206);
#18153=AXIS2_PLACEMENT_3D('',#36329,#21210,#21211);
#18154=AXIS2_PLACEMENT_3D('',#36332,#21214,#21215);
#18155=AXIS2_PLACEMENT_3D('',#36338,#21219,#21220);
#18156=AXIS2_PLACEMENT_3D('',#36344,#21224,#21225);
#18157=AXIS2_PLACEMENT_3D('',#36346,#21227,#21228);
#18158=AXIS2_PLACEMENT_3D('',#36348,#21230,#21231);
#18159=AXIS2_PLACEMENT_3D('',#36350,#21233,#21234);
#18160=AXIS2_PLACEMENT_3D('',#36352,#21235,#21236);
#18161=AXIS2_PLACEMENT_3D('',#36353,#21237,#21238);
#18162=AXIS2_PLACEMENT_3D('',#36356,#21239,#21240);
#18163=AXIS2_PLACEMENT_3D('',#36357,#21241,#21242);
#18164=AXIS2_PLACEMENT_3D('',#36361,#21244,#21245);
#18165=AXIS2_PLACEMENT_3D('',#36362,#21246,#21247);
#18166=AXIS2_PLACEMENT_3D('',#36363,#21248,#21249);
#18167=AXIS2_PLACEMENT_3D('',#36367,#21251,#21252);
#18168=AXIS2_PLACEMENT_3D('',#36368,#21253,#21254);
#18169=AXIS2_PLACEMENT_3D('',#36369,#21255,#21256);
#18170=AXIS2_PLACEMENT_3D('',#36371,#21257,#21258);
#18171=AXIS2_PLACEMENT_3D('',#36373,#21260,#21261);
#18172=AXIS2_PLACEMENT_3D('',#36376,#21263,#21264);
#18173=AXIS2_PLACEMENT_3D('',#36377,#21265,#21266);
#18174=AXIS2_PLACEMENT_3D('',#36378,#21267,#21268);
#18175=AXIS2_PLACEMENT_3D('',#36380,#21269,#21270);
#18176=AXIS2_PLACEMENT_3D('',#36384,#21272,#21273);
#18177=AXIS2_PLACEMENT_3D('',#36385,#21274,#21275);
#18178=AXIS2_PLACEMENT_3D('',#36386,#21276,#21277);
#18179=AXIS2_PLACEMENT_3D('',#36389,#21279,#21280);
#18180=AXIS2_PLACEMENT_3D('',#36390,#21281,#21282);
#18181=AXIS2_PLACEMENT_3D('',#36394,#21286,#21287);
#18182=AXIS2_PLACEMENT_3D('',#36396,#21288,#21289);
#18183=AXIS2_PLACEMENT_3D('',#36397,#21290,#21291);
#18184=AXIS2_PLACEMENT_3D('',#36399,#21292,#21293);
#18185=AXIS2_PLACEMENT_3D('',#36401,#21294,#21295);
#18186=AXIS2_PLACEMENT_3D('',#36402,#21296,#21297);
#18187=AXIS2_PLACEMENT_3D('',#36404,#21299,#21300);
#18188=AXIS2_PLACEMENT_3D('',#36406,#21301,#21302);
#18189=AXIS2_PLACEMENT_3D('',#36408,#21304,#21305);
#18190=AXIS2_PLACEMENT_3D('',#36410,#21306,#21307);
#18191=AXIS2_PLACEMENT_3D('',#36411,#21308,#21309);
#18192=AXIS2_PLACEMENT_3D('',#36413,#21310,#21311);
#18193=AXIS2_PLACEMENT_3D('',#36414,#21312,#21313);
#18194=AXIS2_PLACEMENT_3D('',#36416,#21315,#21316);
#18195=AXIS2_PLACEMENT_3D('',#36417,#21317,#21318);
#18196=AXIS2_PLACEMENT_3D('',#36418,#21319,#21320);
#18197=AXIS2_PLACEMENT_3D('',#36419,#21321,#21322);
#18198=AXIS2_PLACEMENT_3D('',#36421,#21323,#21324);
#18199=AXIS2_PLACEMENT_3D('',#36423,#21326,#21327);
#18200=AXIS2_PLACEMENT_3D('',#36425,#21328,#21329);
#18201=AXIS2_PLACEMENT_3D('',#36427,#21331,#21332);
#21138=DIRECTION('axis',(0.,0.,1.));
#21139=DIRECTION('refdir',(1.,0.,0.));
#21140=DIRECTION('center_axis',(2.1030317852139E-15,-0.547750005235842,
0.836642057133238));
#21141=DIRECTION('ref_axis',(1.,0.,-2.51365774321693E-15));
#21142=DIRECTION('',(1.,0.,-2.56395024851142E-15));
#21143=DIRECTION('',(-0.586730430533741,0.677497944020818,0.443558268701256));
#21144=DIRECTION('',(-0.58673043053375,-0.677497944020814,-0.443558268701251));
#21145=DIRECTION('center_axis',(-0.724553275351853,-0.547750005235845,0.418321028566619));
#21146=DIRECTION('ref_axis',(0.500000000000001,0.,0.866025403784438));
#21147=DIRECTION('',(0.500000000000001,0.,0.866025403784438));
#21148=DIRECTION('',(-0.677497944020805,0.677497944020814,-0.286344323664975));
#21149=DIRECTION('',(0.0907675134870613,-0.677497944020816,-0.72990259236623));
#21150=DIRECTION('center_axis',(0.724553275351854,-0.547750005235844,0.418321028566617));
#21151=DIRECTION('ref_axis',(0.499999999999999,0.,-0.866025403784439));
#21152=DIRECTION('',(0.500000000000003,0.,-0.866025403784437));
#21153=DIRECTION('',(0.0907675134870613,0.677497944020816,0.72990259236623));
#21154=DIRECTION('',(-0.677497944020804,-0.677497944020816,0.286344323664975));
#21155=DIRECTION('center_axis',(0.353553390593277,-0.707106781186542,0.612372435695799));
#21156=DIRECTION('ref_axis',(0.866025403784439,0.,-0.5));
#21157=DIRECTION('',(0.866025403784439,0.,-0.5));
#21158=DIRECTION('',(-0.866025403784439,0.,0.5));
#21159=DIRECTION('center_axis',(-0.724553275351849,-0.547750005235848,-0.418321028566621));
#21160=DIRECTION('ref_axis',(-0.500000000000005,0.,0.866025403784436));
#21161=DIRECTION('',(-0.500000000000002,0.,0.866025403784437));
#21162=DIRECTION('',(-0.0907675134870579,0.677497944020813,-0.729902592366233));
#21163=DIRECTION('',(0.677497944020807,-0.677497944020816,-0.286344323664964));
#21164=DIRECTION('center_axis',(0.724553275351851,-0.547750005235849,-0.418321028566616));
#21165=DIRECTION('ref_axis',(-0.499999999999999,0.,-0.866025403784439));
#21166=DIRECTION('',(0.677497944020806,0.677497944020818,0.286344323664964));
#21167=DIRECTION('',(-0.0907675134870605,-0.67749794402081,0.729902592366236));
#21168=DIRECTION('',(-0.499999999999999,0.,-0.866025403784439));
#21169=DIRECTION('center_axis',(0.,-0.547750005235853,-0.83664205713323));
#21170=DIRECTION('ref_axis',(-1.,0.,0.));
#21171=DIRECTION('',(-1.,0.,0.));
#21172=DIRECTION('',(0.586730430533742,0.677497944020812,-0.443558268701264));
#21173=DIRECTION('',(0.58673043053374,-0.677497944020813,0.443558268701265));
#21174=DIRECTION('center_axis',(0.353553390593275,-0.707106781186545,-0.612372435695797));
#21175=DIRECTION('ref_axis',(-0.866025403784439,0.,-0.499999999999999));
#21176=DIRECTION('',(-0.866025403784439,0.,-0.499999999999999));
#21177=DIRECTION('',(0.866025403784439,0.,0.499999999999999));
#21178=DIRECTION('center_axis',(-0.353553390593275,-0.707106781186544,-0.612372435695797));
#21179=DIRECTION('ref_axis',(-0.866025403784439,0.,0.5));
#21180=DIRECTION('',(-0.866025403784439,0.,0.5));
#21181=DIRECTION('',(0.866025403784439,0.,-0.5));
#21182=DIRECTION('center_axis',(0.,0.,-1.));
#21183=DIRECTION('ref_axis',(-1.,0.,0.));
#21184=DIRECTION('',(-1.,0.,0.));
#21185=DIRECTION('',(0.,-1.,0.));
#21186=DIRECTION('',(0.,1.,0.));
#21187=DIRECTION('center_axis',(0.866025403784439,0.,-0.499999999999999));
#21188=DIRECTION('ref_axis',(-0.499999999999999,0.,-0.866025403784439));
#21189=DIRECTION('',(-0.499999999999999,0.,-0.866025403784439));
#21190=DIRECTION('',(0.,-1.,0.));
#21191=DIRECTION('',(0.,1.,0.));
#21192=DIRECTION('center_axis',(0.707106781186554,-0.707106781186541,0.));
#21193=DIRECTION('ref_axis',(0.,0.,-1.));
#21194=DIRECTION('',(0.,0.,-1.));
#21195=DIRECTION('',(0.,0.,1.));
#21196=DIRECTION('center_axis',(-0.707106781186552,-0.707106781186543,-1.43130521632687E-16));
#21197=DIRECTION('ref_axis',(-2.0241712488248E-16,0.,1.));
#21198=DIRECTION('',(-2.0241712488248E-16,0.,1.));
#21199=DIRECTION('',(2.0241712488248E-16,0.,-1.));
#21200=DIRECTION('center_axis',(-0.866025403784437,0.,-0.500000000000002));
#21201=DIRECTION('ref_axis',(-0.500000000000002,0.,0.866025403784437));
#21202=DIRECTION('',(-0.500000000000002,0.,0.866025403784437));
#21203=DIRECTION('',(0.,-1.,0.));
#21204=DIRECTION('',(0.,1.,0.));
#21205=DIRECTION('center_axis',(0.866025403784437,0.,0.500000000000003));
#21206=DIRECTION('ref_axis',(0.500000000000003,0.,-0.866025403784437));
#21207=DIRECTION('',(0.500000000000003,0.,-0.866025403784437));
#21208=DIRECTION('',(0.,-1.,0.));
#21209=DIRECTION('',(0.,1.,0.));
#21210=DIRECTION('center_axis',(-0.353553390593277,-0.70710678118654,0.612372435695801));
#21211=DIRECTION('ref_axis',(0.866025403784439,0.,0.5));
#21212=DIRECTION('',(0.866025403784439,0.,0.5));
#21213=DIRECTION('',(-0.866025403784439,0.,-0.5));
#21214=DIRECTION('center_axis',(-0.866025403784438,0.,0.500000000000001));
#21215=DIRECTION('ref_axis',(0.500000000000001,0.,0.866025403784438));
#21216=DIRECTION('',(0.500000000000001,0.,0.866025403784438));
#21217=DIRECTION('',(0.,-1.,0.));
#21218=DIRECTION('',(0.,1.,0.));
#21219=DIRECTION('center_axis',(2.56395024851142E-15,0.,1.));
#21220=DIRECTION('ref_axis',(1.,0.,-2.56395024851142E-15));
#21221=DIRECTION('',(1.,0.,-2.56395024851142E-15));
#21222=DIRECTION('',(0.,-1.,0.));
#21223=DIRECTION('',(0.,1.,0.));
#21224=DIRECTION('center_axis',(-0.5,0.,-0.866025403784439));
#21225=DIRECTION('ref_axis',(-0.866025403784439,0.,0.5));
#21226=DIRECTION('',(-0.866025403784439,0.,0.5));
#21227=DIRECTION('center_axis',(-1.,0.,-2.0241712488248E-16));
#21228=DIRECTION('ref_axis',(-2.0241712488248E-16,0.,1.));
#21229=DIRECTION('',(-2.0241712488248E-16,0.,1.));
#21230=DIRECTION('center_axis',(-0.5,0.,0.866025403784439));
#21231=DIRECTION('ref_axis',(0.866025403784439,0.,0.5));
#21232=DIRECTION('',(0.866025403784439,0.,0.5));
#21233=DIRECTION('center_axis',(0.,1.,0.));
#21234=DIRECTION('ref_axis',(1.,0.,0.));
#21235=DIRECTION('center_axis',(0.,-1.,0.));
#21236=DIRECTION('ref_axis',(1.,0.,0.));
#21237=DIRECTION('center_axis',(0.,-1.,0.));
#21238=DIRECTION('ref_axis',(-1.,0.,0.));
#21239=DIRECTION('center_axis',(0.,1.,0.));
#21240=DIRECTION('ref_axis',(-1.,0.,0.));
#21241=DIRECTION('center_axis',(0.,1.,0.));
#21242=DIRECTION('ref_axis',(-1.,0.,0.));
#21243=DIRECTION('',(-0.382683432365081,0.923879532511291,-4.68652040532618E-17));
#21244=DIRECTION('center_axis',(0.,-1.,0.));
#21245=DIRECTION('ref_axis',(-1.,0.,0.));
#21246=DIRECTION('center_axis',(0.,-1.,0.));
#21247=DIRECTION('ref_axis',(-1.,0.,0.));
#21248=DIRECTION('center_axis',(0.,-1.,0.));
#21249=DIRECTION('ref_axis',(1.,0.,0.));
#21250=DIRECTION('',(0.707106781186546,0.707106781186549,8.65956056235492E-17));
#21251=DIRECTION('center_axis',(0.,1.,0.));
#21252=DIRECTION('ref_axis',(-1.,0.,0.));
#21253=DIRECTION('center_axis',(0.,1.,0.));
#21254=DIRECTION('ref_axis',(-1.,0.,0.));
#21255=DIRECTION('center_axis',(0.,-1.,0.));
#21256=DIRECTION('ref_axis',(1.,0.,0.));
#21257=DIRECTION('center_axis',(0.,1.,0.));
#21258=DIRECTION('ref_axis',(1.,0.,0.));
#21259=DIRECTION('',(0.,1.,0.));
#21260=DIRECTION('center_axis',(0.,-1.,0.));
#21261=DIRECTION('ref_axis',(-1.,0.,0.));
#21262=DIRECTION('',(-0.923879532511288,0.382683432365086,-1.1314261122877E-16));
#21263=DIRECTION('center_axis',(0.,-1.,0.));
#21264=DIRECTION('ref_axis',(-1.,0.,0.));
#21265=DIRECTION('center_axis',(0.,1.,0.));
#21266=DIRECTION('ref_axis',(0.,0.,1.));
#21267=DIRECTION('center_axis',(0.,1.,0.));
#21268=DIRECTION('ref_axis',(-1.,0.,0.));
#21269=DIRECTION('center_axis',(0.,1.,0.));
#21270=DIRECTION('ref_axis',(-1.,0.,0.));
#21271=DIRECTION('',(0.707106781186549,0.707106781186546,8.65956056235495E-17));
#21272=DIRECTION('center_axis',(0.,-1.,0.));
#21273=DIRECTION('ref_axis',(-1.,0.,0.));
#21274=DIRECTION('center_axis',(0.,-1.,0.));
#21275=DIRECTION('ref_axis',(-1.,0.,0.));
#21276=DIRECTION('center_axis',(0.,-1.,0.));
#21277=DIRECTION('ref_axis',(1.,0.,0.));
#21278=DIRECTION('',(0.,1.,0.));
#21279=DIRECTION('center_axis',(0.,-1.,0.));
#21280=DIRECTION('ref_axis',(1.,0.,0.));
#21281=DIRECTION('center_axis',(0.,-1.,0.));
#21282=DIRECTION('ref_axis',(0.,0.,-1.));
#21283=DIRECTION('',(0.,0.,-1.));
#21284=DIRECTION('',(-0.866025403784439,0.,-0.499999999999999));
#21285=DIRECTION('',(0.866025403784439,0.,-0.5));
#21286=DIRECTION('center_axis',(0.,1.,0.));
#21287=DIRECTION('ref_axis',(0.,0.,1.));
#21288=DIRECTION('center_axis',(0.,-1.,0.));
#21289=DIRECTION('ref_axis',(1.,0.,0.));
#21290=DIRECTION('center_axis',(0.,-1.,0.));
#21291=DIRECTION('ref_axis',(0.,0.,-1.));
#21292=DIRECTION('center_axis',(0.,-1.,0.));
#21293=DIRECTION('ref_axis',(1.,0.,0.));
#21294=DIRECTION('center_axis',(0.,-1.,0.));
#21295=DIRECTION('ref_axis',(1.,0.,0.));
#21296=DIRECTION('center_axis',(0.,-1.,0.));
#21297=DIRECTION('ref_axis',(1.,0.,0.));
#21298=DIRECTION('',(0.,-1.,0.));
#21299=DIRECTION('center_axis',(0.,-1.,0.));
#21300=DIRECTION('ref_axis',(1.,0.,0.));
#21301=DIRECTION('center_axis',(0.,1.,0.));
#21302=DIRECTION('ref_axis',(1.,0.,0.));
#21303=DIRECTION('',(0.,1.,0.));
#21304=DIRECTION('center_axis',(0.,1.,0.));
#21305=DIRECTION('ref_axis',(0.,0.,1.));
#21306=DIRECTION('center_axis',(0.,-1.,0.));
#21307=DIRECTION('ref_axis',(1.,0.,0.));
#21308=DIRECTION('center_axis',(0.,-1.,0.));
#21309=DIRECTION('ref_axis',(0.,0.,-1.));
#21310=DIRECTION('center_axis',(0.,-1.,0.));
#21311=DIRECTION('ref_axis',(1.,0.,0.));
#21312=DIRECTION('center_axis',(0.,-1.,0.));
#21313=DIRECTION('ref_axis',(1.,0.,0.));
#21314=DIRECTION('',(0.,-1.,0.));
#21315=DIRECTION('center_axis',(1.,0.,0.));
#21316=DIRECTION('ref_axis',(0.,0.,-1.));
#21317=DIRECTION('center_axis',(0.5,0.,0.866025403784439));
#21318=DIRECTION('ref_axis',(0.866025403784439,0.,-0.5));
#21319=DIRECTION('center_axis',(0.5,0.,-0.866025403784439));
#21320=DIRECTION('ref_axis',(-0.866025403784439,0.,-0.499999999999999));
#21321=DIRECTION('center_axis',(0.,-1.,0.));
#21322=DIRECTION('ref_axis',(1.,0.,0.));
#21323=DIRECTION('center_axis',(0.,-1.,0.));
#21324=DIRECTION('ref_axis',(1.,0.,0.));
#21325=DIRECTION('',(0.,1.,0.));
#21326=DIRECTION('center_axis',(0.,1.,0.));
#21327=DIRECTION('ref_axis',(1.,0.,0.));
#21328=DIRECTION('center_axis',(0.,-1.,0.));
#21329=DIRECTION('ref_axis',(1.,0.,0.));
#21330=DIRECTION('',(-0.514495755427524,0.857492925712546,-6.30075580059217E-17));
#21331=DIRECTION('center_axis',(0.,-1.,0.));
#21332=DIRECTION('ref_axis',(0.,0.,-1.));
#36247=CARTESIAN_POINT('',(0.,0.,0.));
#36248=CARTESIAN_POINT('Origin',(16.,70.,-17.6076951545867));
#36249=CARTESIAN_POINT('',(15.5669872981078,70.5,-17.2803448853971));
#36250=CARTESIAN_POINT('',(16.4330127018922,70.5,-17.2803448853971));
#36251=CARTESIAN_POINT('',(15.5669872981078,70.5,-17.2803448853971));
#36252=CARTESIAN_POINT('',(16.,70.,-17.6076951545867));
#36253=CARTESIAN_POINT('',(16.,70.,-17.6076951545867));
#36254=CARTESIAN_POINT('',(16.4330127018922,70.5,-17.2803448853971));
#36255=CARTESIAN_POINT('Origin',(7.,70.,-22.8038475772934));
#36256=CARTESIAN_POINT('',(6.5,70.5,-23.0151724426986));
#36257=CARTESIAN_POINT('',(6.93301270189222,70.5,-22.2651724426986));
#36258=CARTESIAN_POINT('',(6.5,70.5,-23.0151724426986));
#36259=CARTESIAN_POINT('',(7.,70.,-22.8038475772934));
#36260=CARTESIAN_POINT('',(7.,70.,-22.8038475772934));
#36261=CARTESIAN_POINT('',(6.93301270189222,70.5,-22.2651724426986));
#36262=CARTESIAN_POINT('Origin',(25.,70.,-22.8038475772934));
#36263=CARTESIAN_POINT('',(25.0669872981078,70.5,-22.2651724426986));
#36264=CARTESIAN_POINT('',(25.5,70.5,-23.0151724426986));
#36265=CARTESIAN_POINT('',(25.0669872981078,70.5,-22.2651724426986));
#36266=CARTESIAN_POINT('',(25.,70.,-22.8038475772934));
#36267=CARTESIAN_POINT('',(25.,70.,-22.8038475772934));
#36268=CARTESIAN_POINT('',(25.5,70.5,-23.0151724426986));
#36269=CARTESIAN_POINT('Origin',(18.25,70.25,-18.6180581256686));
#36270=CARTESIAN_POINT('',(18.125,70.,-18.8345644766147));
#36271=CARTESIAN_POINT('',(18.375,70.5,-18.4015517747225));
#36272=CARTESIAN_POINT('Origin',(7.,70.,-33.1961524227066));
#36273=CARTESIAN_POINT('',(6.93301270189222,70.5,-33.7348275573014));
#36274=CARTESIAN_POINT('',(6.5,70.5,-32.9848275573015));
#36275=CARTESIAN_POINT('',(6.93301270189222,70.5,-33.7348275573015));
#36276=CARTESIAN_POINT('',(7.,70.,-33.1961524227066));
#36277=CARTESIAN_POINT('',(7.,70.,-33.1961524227066));
#36278=CARTESIAN_POINT('',(6.5,70.5,-32.9848275573015));
#36279=CARTESIAN_POINT('Origin',(25.0669872981078,70.5,-33.7348275573015));
#36280=CARTESIAN_POINT('',(25.,70.,-33.1961524227066));
#36281=CARTESIAN_POINT('',(25.5,70.5,-32.9848275573015));
#36282=CARTESIAN_POINT('',(25.,70.,-33.1961524227066));
#36283=CARTESIAN_POINT('',(25.0669872981078,70.5,-33.7348275573015));
#36284=CARTESIAN_POINT('',(25.0669872981078,70.5,-33.7348275573015));
#36285=CARTESIAN_POINT('',(25.5,70.5,-32.9848275573015));
#36286=CARTESIAN_POINT('Origin',(16.,70.,-38.3923048454133));
#36287=CARTESIAN_POINT('',(16.4330127018922,70.5,-38.7196551146029));
#36288=CARTESIAN_POINT('',(15.5669872981078,70.5,-38.7196551146029));
#36289=CARTESIAN_POINT('',(16.4330127018922,70.5,-38.7196551146029));
#36290=CARTESIAN_POINT('',(16.,70.,-38.3923048454133));
#36291=CARTESIAN_POINT('',(16.,70.,-38.3923048454133));
#36292=CARTESIAN_POINT('',(15.5669872981078,70.5,-38.7196551146029));
#36293=CARTESIAN_POINT('Origin',(23.,70.25,-34.6395280956807));
#36294=CARTESIAN_POINT('',(22.875,70.,-34.4230217447346));
#36295=CARTESIAN_POINT('',(23.125,70.5,-34.8560344466268));
#36296=CARTESIAN_POINT('Origin',(13.75,70.25,-37.3819418743314));
#36297=CARTESIAN_POINT('',(13.875,70.,-37.1654355233853));
#36298=CARTESIAN_POINT('',(13.625,70.5,-37.5984482252775));
#36299=CARTESIAN_POINT('Origin',(16.,70.,-38.7196551146029));
#36300=CARTESIAN_POINT('',(15.5669872981078,74.,-38.7196551146029));
#36301=CARTESIAN_POINT('',(16.4330127018922,74.,-38.7196551146029));
#36302=CARTESIAN_POINT('',(16.,74.,-38.7196551146029));
#36303=CARTESIAN_POINT('',(16.4330127018922,70.,-38.7196551146029));
#36304=CARTESIAN_POINT('',(15.5669872981078,70.,-38.7196551146029));
#36305=CARTESIAN_POINT('Origin',(25.2834936490539,70.,-33.3598275573014));
#36306=CARTESIAN_POINT('',(25.0669872981078,74.,-33.7348275573015));
#36307=CARTESIAN_POINT('',(25.5,74.,-32.9848275573015));
#36308=CARTESIAN_POINT('',(25.2834936490539,74.,-33.3598275573014));
#36309=CARTESIAN_POINT('',(25.5,70.,-32.9848275573015));
#36310=CARTESIAN_POINT('',(25.0669872981078,70.,-33.7348275573015));
#36311=CARTESIAN_POINT('Origin',(25.25,70.25,-25.2575862213493));
#36312=CARTESIAN_POINT('',(25.,70.,-25.2575862213493));
#36313=CARTESIAN_POINT('',(25.5,70.5,-25.2575862213493));
#36314=CARTESIAN_POINT('Origin',(6.75,70.25,-30.7424137786507));
#36315=CARTESIAN_POINT('',(7.,70.,-30.7424137786507));
#36316=CARTESIAN_POINT('',(6.5,70.5,-30.7424137786507));
#36317=CARTESIAN_POINT('Origin',(6.71650635094611,70.,-33.3598275573014));
#36318=CARTESIAN_POINT('',(6.5,74.,-32.9848275573015));
#36319=CARTESIAN_POINT('',(6.93301270189222,74.,-33.7348275573014));
#36320=CARTESIAN_POINT('',(6.71650635094611,74.,-33.3598275573015));
#36321=CARTESIAN_POINT('',(6.93301270189222,70.,-33.7348275573015));
#36322=CARTESIAN_POINT('',(6.5,70.,-32.9848275573015));
#36323=CARTESIAN_POINT('Origin',(25.2834936490539,70.,-22.6401724426986));
#36324=CARTESIAN_POINT('',(25.5,74.,-23.0151724426986));
#36325=CARTESIAN_POINT('',(25.0669872981078,74.,-22.2651724426986));
#36326=CARTESIAN_POINT('',(25.2834936490539,74.,-22.6401724426985));
#36327=CARTESIAN_POINT('',(25.0669872981078,70.,-22.2651724426986));
#36328=CARTESIAN_POINT('',(25.5,70.,-23.0151724426986));
#36329=CARTESIAN_POINT('Origin',(9.,70.25,-21.3604719043193));
#36330=CARTESIAN_POINT('',(9.125,70.,-21.5769782552654));
#36331=CARTESIAN_POINT('',(8.875,70.5,-21.1439655533732));
#36332=CARTESIAN_POINT('Origin',(6.71650635094611,70.,-22.6401724426986));
#36333=CARTESIAN_POINT('',(6.93301270189222,74.,-22.2651724426986));
#36334=CARTESIAN_POINT('',(6.5,74.,-23.0151724426986));
#36335=CARTESIAN_POINT('',(6.71650635094611,74.,-22.6401724426985));
#36336=CARTESIAN_POINT('',(6.5,70.,-23.0151724426986));
#36337=CARTESIAN_POINT('',(6.93301270189222,70.,-22.2651724426986));
#36338=CARTESIAN_POINT('Origin',(16.,70.,-17.2803448853971));
#36339=CARTESIAN_POINT('',(16.4330127018922,74.,-17.2803448853971));
#36340=CARTESIAN_POINT('',(15.5669872981078,74.,-17.2803448853971));
#36341=CARTESIAN_POINT('',(16.,74.,-17.2803448853971));
#36342=CARTESIAN_POINT('',(15.5669872981078,70.,-17.2803448853971));
#36343=CARTESIAN_POINT('',(16.4330127018922,70.,-17.2803448853971));
#36344=CARTESIAN_POINT('Origin',(16.,70.,-38.9696551146029));
#36345=CARTESIAN_POINT('',(6.5,74.,-33.4848275573014));
#36346=CARTESIAN_POINT('Origin',(6.5,70.,-33.4848275573014));
#36347=CARTESIAN_POINT('',(6.5,74.,-22.5151724426986));
#36348=CARTESIAN_POINT('Origin',(6.5,70.,-22.5151724426986));
#36349=CARTESIAN_POINT('',(16.,74.,-17.0303448853971));
#36350=CARTESIAN_POINT('Origin',(16.,70.,-28.));
#36351=CARTESIAN_POINT('',(7.5,70.,-28.));
#36352=CARTESIAN_POINT('Origin',(16.,70.,-28.));
#36353=CARTESIAN_POINT('Origin',(16.,81.4267766952966,-28.));
#36354=CARTESIAN_POINT('',(28.,81.,-28.));
#36355=CARTESIAN_POINT('',(4.,81.,-28.));
#36356=CARTESIAN_POINT('Origin',(16.,81.,-28.));
#36357=CARTESIAN_POINT('Origin',(16.,81.,-28.));
#36358=CARTESIAN_POINT('',(27.6464466094067,81.8535533905933,-28.));
#36359=CARTESIAN_POINT('',(27.8232233047034,81.4267766952966,-28.));
#36360=CARTESIAN_POINT('',(4.35355339059327,81.8535533905933,-28.));
#36361=CARTESIAN_POINT('Origin',(16.,81.8535533905933,-28.));
#36362=CARTESIAN_POINT('Origin',(16.,81.8535533905933,-28.));
#36363=CARTESIAN_POINT('Origin',(16.,82.25,-28.));
#36364=CARTESIAN_POINT('',(5.14644660940672,82.6464466094067,-28.));
#36365=CARTESIAN_POINT('',(4.75000000000001,82.25,-28.));
#36366=CARTESIAN_POINT('',(26.8535533905933,82.6464466094067,-28.));
#36367=CARTESIAN_POINT('Origin',(16.,82.6464466094067,-28.));
#36368=CARTESIAN_POINT('Origin',(16.,82.6464466094067,-28.));
#36369=CARTESIAN_POINT('Origin',(16.,77.75,-28.));
#36370=CARTESIAN_POINT('',(4.,79.7,-28.));
#36371=CARTESIAN_POINT('Origin',(16.,79.7,-28.));
#36372=CARTESIAN_POINT('',(4.,77.75,-28.));
#36373=CARTESIAN_POINT('Origin',(16.,82.8232233047034,-28.));
#36374=CARTESIAN_POINT('',(26.,83.,-28.));
#36375=CARTESIAN_POINT('',(26.4267766952966,82.8232233047034,-28.));
#36376=CARTESIAN_POINT('Origin',(16.,83.,-28.));
#36377=CARTESIAN_POINT('Origin',(26.5,83.,-28.));
#36378=CARTESIAN_POINT('Origin',(16.,74.25,-28.));
#36379=CARTESIAN_POINT('',(27.5,74.,-28.));
#36380=CARTESIAN_POINT('Origin',(16.,74.,-28.));
#36381=CARTESIAN_POINT('',(28.,74.5,-28.));
#36382=CARTESIAN_POINT('',(27.75,74.25,-28.));
#36383=CARTESIAN_POINT('',(4.,74.5,-28.));
#36384=CARTESIAN_POINT('Origin',(16.,74.5,-28.));
#36385=CARTESIAN_POINT('Origin',(16.,74.5,-28.));
#36386=CARTESIAN_POINT('Origin',(16.,77.75,-28.));
#36387=CARTESIAN_POINT('',(4.,75.5,-28.));
#36388=CARTESIAN_POINT('',(4.,77.75,-28.));
#36389=CARTESIAN_POINT('Origin',(16.,75.5,-28.));
#36390=CARTESIAN_POINT('Origin',(16.,74.,-28.));
#36391=CARTESIAN_POINT('',(25.5,74.,-33.4848275573015));
#36392=CARTESIAN_POINT('',(16.,74.,-38.9696551146029));
#36393=CARTESIAN_POINT('',(25.5,74.,-22.5151724426986));
#36394=CARTESIAN_POINT('Origin',(28.1,79.7,-28.));
#36395=CARTESIAN_POINT('',(5.,79.7,-28.));
#36396=CARTESIAN_POINT('Origin',(16.,79.7,-28.));
#36397=CARTESIAN_POINT('Origin',(27.,78.5,-28.));
#36398=CARTESIAN_POINT('',(4.,78.5,-28.));
#36399=CARTESIAN_POINT('Origin',(16.,78.5,-28.));
#36400=CARTESIAN_POINT('',(5.,78.5,-28.));
#36401=CARTESIAN_POINT('Origin',(16.,78.5,-28.));
#36402=CARTESIAN_POINT('Origin',(16.,79.1,-28.));
#36403=CARTESIAN_POINT('',(5.,79.1,-28.));
#36404=CARTESIAN_POINT('Origin',(16.,77.75,-28.));
#36405=CARTESIAN_POINT('',(4.,76.7,-28.));
#36406=CARTESIAN_POINT('Origin',(16.,76.7,-28.));
#36407=CARTESIAN_POINT('',(4.,77.75,-28.));
#36408=CARTESIAN_POINT('Origin',(28.1,76.7,-28.));
#36409=CARTESIAN_POINT('',(5.,76.7,-28.));
#36410=CARTESIAN_POINT('Origin',(16.,76.7,-28.));
#36411=CARTESIAN_POINT('Origin',(27.,75.5,-28.));
#36412=CARTESIAN_POINT('',(5.,75.5,-28.));
#36413=CARTESIAN_POINT('Origin',(16.,75.5,-28.));
#36414=CARTESIAN_POINT('Origin',(16.,76.1,-28.));
#36415=CARTESIAN_POINT('',(5.,76.1,-28.));
#36416=CARTESIAN_POINT('Origin',(25.5,70.,-22.5151724426986));
#36417=CARTESIAN_POINT('Origin',(16.,70.,-17.0303448853971));
#36418=CARTESIAN_POINT('Origin',(25.5,70.,-33.4848275573015));
#36419=CARTESIAN_POINT('Origin',(16.,64.5,-28.));
#36420=CARTESIAN_POINT('',(7.5,59.,-28.));
#36421=CARTESIAN_POINT('Origin',(16.,59.,-28.));
#36422=CARTESIAN_POINT('',(7.5,64.5,-28.));
#36423=CARTESIAN_POINT('Origin',(16.,58.75,-28.));
#36424=CARTESIAN_POINT('',(7.8,58.5,-28.));
#36425=CARTESIAN_POINT('Origin',(16.,58.5,-28.));
#36426=CARTESIAN_POINT('',(7.65,58.75,-28.));
#36427=CARTESIAN_POINT('Origin',(16.,58.5,-28.));
#56609=UNCERTAINTY_MEASURE_WITH_UNIT(LENGTH_MEASURE(0.01),#56640,
'DISTANCE_ACCURACY_VALUE',
'Maximum model space distance between geometric entities at asserted c
onnectivities');
#56617=UNCERTAINTY_MEASURE_WITH_UNIT(LENGTH_MEASURE(0.01),#56640,
'DISTANCE_ACCURACY_VALUE',
'Maximum model space distance between geometric entities at asserted c
onnectivities');
#56631=(
GEOMETRIC_REPRESENTATION_CONTEXT(3)
GLOBAL_UNCERTAINTY_ASSIGNED_CONTEXT((#56609))
GLOBAL_UNIT_ASSIGNED_CONTEXT((#56640,#56642,#56643))
REPRESENTATION_CONTEXT('','3D')
);
#56639=(
GEOMETRIC_REPRESENTATION_CONTEXT(3)
GLOBAL_UNCERTAINTY_ASSIGNED_CONTEXT((#56617))
GLOBAL_UNIT_ASSIGNED_CONTEXT((#56640,#56642,#56643))
REPRESENTATION_CONTEXT('','3D')
);
#56640=(
LENGTH_UNIT()
NAMED_UNIT(*)
SI_UNIT(.MILLI.,.METRE.)
);
#56642=(
NAMED_UNIT(*)
PLANE_ANGLE_UNIT()
SI_UNIT($,.RADIAN.)
);
#56643=(
NAMED_UNIT(*)
SI_UNIT($,.STERADIAN.)
SOLID_ANGLE_UNIT()
);
#56657=SHAPE_DEFINITION_REPRESENTATION(#56678,#56757);
#56678=PRODUCT_DEFINITION_SHAPE('',$,#56779);
#56757=SHAPE_REPRESENTATION('',(#18137),#56631);
#56765=PRODUCT_DEFINITION_CONTEXT('part definition',#56830,'design');
#56779=PRODUCT_DEFINITION('2026-10-26-00-03-01-283',
'20_Exhaust_Silencer_3-8',#56800,#56765);
#56800=PRODUCT_DEFINITION_FORMATION('',$,#56845);
#56830=APPLICATION_CONTEXT(
'Core Data for Automotive Mechanical Design Process');
#56831=PRODUCT_CONTEXT('part definition',#56830,'mechanical');
#56845=PRODUCT('2026-10-26-00-03-01-283','20_Exhaust_Silencer_3-8',$,(#56831));
#56895=COLOUR_RGB('Light Blue',0.38,0.62,0.78);
#56896=FILL_AREA_STYLE_COLOUR('',#56895);
#56897=FILL_AREA_STYLE('',(#56896));
#56898=SURFACE_STYLE_FILL_AREA(#56897);
#56899=SURFACE_SIDE_STYLE('',(#56898));
#56900=SURFACE_STYLE_USAGE(.BOTH.,#56899);
#56901=PRESENTATION_STYLE_ASSIGNMENT((#56900));
ENDSEC;
END-ISO-10303-21;
